ISO-10303-21;
HEADER;
/* Generated by software containing ST-Developer
 * from STEP Tools, Inc. (www.steptools.com) 
 */

FILE_DESCRIPTION(
/* description */ ('Independent two-stage fixed-ring planetary gearbox,24/24/72 teeth,mod
ule2,20deg involutes,three planets per stage,4:1 x4:1=16:1. Native cut
-space/fillet/pattern tooth profiles derived from reusable gear blanks
; shared sun/planet/ring/carrier parts across both stages. Captured br
onze-journal input/carriers, headed retained planet pins, keyed inters
tage drive and modular keyed output interface. Native ideal gear links
; no torque, precision grade, production backlash/fits, lubrication, s
peed or life rating.'),
/* implementation_level */ '2;1');

FILE_NAME(
/* name */ 'Sun thrust washer.step',
/* time_stamp */ '2026-11-08T19:10:00-08:00',
/* author */ (''),
/* organization */ (''),
/* preprocessor_version */ 'ST-DEVELOPER v20.2',
/* originating_system */ 'Autodesk Translation Framework v15.17.0.0',
/* authorisation */ '');

FILE_SCHEMA (('AUTOMOTIVE_DESIGN { 1 0 10303 214 3 1 1 }'));
ENDSEC;

DATA;
#10=MECHANICAL_DESIGN_GEOMETRIC_PRESENTATION_REPRESENTATION('',(#1177),#259224);
#1137=SHAPE_REPRESENTATION_RELATIONSHIP('SRR','None',#259384,#1157);
#1157=ADVANCED_BREP_SHAPE_REPRESENTATION('',(#1197),#259218);
#1177=STYLED_ITEM('',(#259485),#1197);
#1197=MANIFOLD_SOLID_BREP('Body1',#25164);
#1312=FACE_BOUND('',#4424,.T.);
#1313=FACE_BOUND('',#4426,.T.);
#1674=PLANE('',#27137);
#1675=PLANE('',#27138);
#2966=FACE_OUTER_BOUND('',#4421,.T.);
#2967=FACE_OUTER_BOUND('',#4422,.T.);
#2968=FACE_OUTER_BOUND('',#4423,.T.);
#2969=FACE_OUTER_BOUND('',#4425,.T.);
#4421=EDGE_LOOP('',(#22694,#22695,#22696,#22697));
#4422=EDGE_LOOP('',(#22698,#22699,#22700,#22701));
#4423=EDGE_LOOP('',(#22702));
#4424=EDGE_LOOP('',(#22703));
#4425=EDGE_LOOP('',(#22704));
#4426=EDGE_LOOP('',(#22705));
#5361=CIRCLE('',#27132,8.);
#5362=CIRCLE('',#27133,8.);
#5363=CIRCLE('',#27135,11.);
#5364=CIRCLE('',#27136,11.);
#7772=LINE('',#256020,#8957);
#7773=LINE('',#256026,#8958);
#8957=VECTOR('',#31923,8.);
#8958=VECTOR('',#31930,11.);
#11469=VERTEX_POINT('',#256017);
#11470=VERTEX_POINT('',#256019);
#11471=VERTEX_POINT('',#256023);
#11472=VERTEX_POINT('',#256025);
#15232=EDGE_CURVE('',#11469,#11469,#5361,.T.);
#15233=EDGE_CURVE('',#11469,#11470,#7772,.T.);
#15234=EDGE_CURVE('',#11470,#11470,#5362,.T.);
#15235=EDGE_CURVE('',#11471,#11471,#5363,.T.);
#15236=EDGE_CURVE('',#11471,#11472,#7773,.T.);
#15237=EDGE_CURVE('',#11472,#11472,#5364,.T.);
#22694=ORIENTED_EDGE('',*,*,#15232,.F.);
#22695=ORIENTED_EDGE('',*,*,#15233,.T.);
#22696=ORIENTED_EDGE('',*,*,#15234,.T.);
#22697=ORIENTED_EDGE('',*,*,#15233,.F.);
#22698=ORIENTED_EDGE('',*,*,#15235,.F.);
#22699=ORIENTED_EDGE('',*,*,#15236,.T.);
#22700=ORIENTED_EDGE('',*,*,#15237,.T.);
#22701=ORIENTED_EDGE('',*,*,#15236,.F.);
#22702=ORIENTED_EDGE('',*,*,#15235,.T.);
#22703=ORIENTED_EDGE('',*,*,#15232,.T.);
#22704=ORIENTED_EDGE('',*,*,#15237,.F.);
#22705=ORIENTED_EDGE('',*,*,#15234,.F.);
#23752=CYLINDRICAL_SURFACE('',#27131,8.);
#23753=CYLINDRICAL_SURFACE('',#27134,11.);
#25072=ADVANCED_FACE('',(#2966),#23752,.F.);
#25073=ADVANCED_FACE('',(#2967),#23753,.T.);
#25074=ADVANCED_FACE('',(#2968,#1312),#1674,.T.);
#25075=ADVANCED_FACE('',(#2969,#1313),#1675,.F.);
#25164=CLOSED_SHELL('',(#25072,#25073,#25074,#25075));
#27130=AXIS2_PLACEMENT_3D('',#256015,#31917,#31918);
#27131=AXIS2_PLACEMENT_3D('',#256016,#31919,#31920);
#27132=AXIS2_PLACEMENT_3D('',#256018,#31921,#31922);
#27133=AXIS2_PLACEMENT_3D('',#256021,#31924,#31925);
#27134=AXIS2_PLACEMENT_3D('',#256022,#31926,#31927);
#27135=AXIS2_PLACEMENT_3D('',#256024,#31928,#31929);
#27136=AXIS2_PLACEMENT_3D('',#256027,#31931,#31932);
#27137=AXIS2_PLACEMENT_3D('',#256028,#31933,#31934);
#27138=AXIS2_PLACEMENT_3D('',#256029,#31935,#31936);
#31917=DIRECTION('axis',(0.,0.,1.));
#31918=DIRECTION('refdir',(1.,0.,0.));
#31919=DIRECTION('center_axis',(0.,0.,1.));
#31920=DIRECTION('ref_axis',(1.,0.,0.));
#31921=DIRECTION('center_axis',(0.,0.,-1.));
#31922=DIRECTION('ref_axis',(1.,0.,0.));
#31923=DIRECTION('',(0.,0.,-1.));
#31924=DIRECTION('center_axis',(0.,0.,-1.));
#31925=DIRECTION('ref_axis',(1.,0.,0.));
#31926=DIRECTION('center_axis',(0.,0.,1.));
#31927=DIRECTION('ref_axis',(1.,0.,0.));
#31928=DIRECTION('center_axis',(0.,0.,1.));
#31929=DIRECTION('ref_axis',(1.,0.,0.));
#31930=DIRECTION('',(0.,0.,-1.));
#31931=DIRECTION('center_axis',(0.,0.,1.));
#31932=DIRECTION('ref_axis',(1.,0.,0.));
#31933=DIRECTION('center_axis',(0.,0.,1.));
#31934=DIRECTION('ref_axis',(1.,0.,0.));
#31935=DIRECTION('center_axis',(0.,0.,1.));
#31936=DIRECTION('ref_axis',(1.,0.,0.));
#256015=CARTESIAN_POINT('',(0.,0.,0.));
#256016=CARTESIAN_POINT('Origin',(0.,0.,0.));
#256017=CARTESIAN_POINT('',(-8.,-9.79717439317883E-16,2.));
#256018=CARTESIAN_POINT('Origin',(0.,0.,2.));
#256019=CARTESIAN_POINT('',(-8.,-9.79717439317883E-16,0.));
#256020=CARTESIAN_POINT('',(-8.,-9.79717439317883E-16,0.));
#256021=CARTESIAN_POINT('Origin',(0.,0.,0.));
#256022=CARTESIAN_POINT('Origin',(0.,0.,0.));
#256023=CARTESIAN_POINT('',(-11.,-1.34711147906209E-15,2.));
#256024=CARTESIAN_POINT('Origin',(0.,0.,2.));
#256025=CARTESIAN_POINT('',(-11.,-1.34711147906209E-15,0.));
#256026=CARTESIAN_POINT('',(-11.,-1.34711147906209E-15,0.));
#256027=CARTESIAN_POINT('Origin',(0.,0.,0.));
#256028=CARTESIAN_POINT('Origin',(0.,0.,2.));
#256029=CARTESIAN_POINT('Origin',(0.,0.,0.));
#259196=UNCERTAINTY_MEASURE_WITH_UNIT(LENGTH_MEASURE(0.01),#259225,
'DISTANCE_ACCURACY_VALUE',
'Maximum model space distance between geometric entities at asserted c
onnectivities');
#259202=UNCERTAINTY_MEASURE_WITH_UNIT(LENGTH_MEASURE(0.01),#259225,
'DISTANCE_ACCURACY_VALUE',
'Maximum model space distance between geometric entities at asserted c
onnectivities');
#259218=(
GEOMETRIC_REPRESENTATION_CONTEXT(3)
GLOBAL_UNCERTAINTY_ASSIGNED_CONTEXT((#259196))
GLOBAL_UNIT_ASSIGNED_CONTEXT((#259225,#259227,#259228))
REPRESENTATION_CONTEXT('','3D')
);
#259224=(
GEOMETRIC_REPRESENTATION_CONTEXT(3)
GLOBAL_UNCERTAINTY_ASSIGNED_CONTEXT((#259202))
GLOBAL_UNIT_ASSIGNED_CONTEXT((#259225,#259227,#259228))
REPRESENTATION_CONTEXT('','3D')
);
#259225=(
LENGTH_UNIT()
NAMED_UNIT(*)
SI_UNIT(.MILLI.,.METRE.)
);
#259227=(
NAMED_UNIT(*)
PLANE_ANGLE_UNIT()
SI_UNIT($,.RADIAN.)
);
#259228=(
NAMED_UNIT(*)
SI_UNIT($,.STERADIAN.)
SOLID_ANGLE_UNIT()
);
#259244=SHAPE_DEFINITION_REPRESENTATION(#259265,#259384);
#259265=PRODUCT_DEFINITION_SHAPE('',$,#259406);
#259384=SHAPE_REPRESENTATION('',(#27130),#259218);
#259390=PRODUCT_DEFINITION_CONTEXT('part definition',#259455,'design');
#259406=PRODUCT_DEFINITION('Sun thrust washer','Sun thrust washer',#259427,
#259390);
#259427=PRODUCT_DEFINITION_FORMATION('',$,#259472);
#259455=APPLICATION_CONTEXT(
'Core Data for Automotive Mechanical Design Process');
#259456=PRODUCT_CONTEXT('part definition',#259455,'mechanical');
#259472=PRODUCT('Sun thrust washer','Sun thrust washer',$,(#259456));
#259485=PRESENTATION_STYLE_ASSIGNMENT((#259500));
#259500=SURFACE_STYLE_USAGE(.BOTH.,#259515);
#259515=SURFACE_SIDE_STYLE('',(#259530));
#259530=SURFACE_STYLE_FILL_AREA(#259545);
#259545=FILL_AREA_STYLE('Bearing light gray',(#259560));
#259560=FILL_AREA_STYLE_COLOUR('Bearing light gray',#259575);
#259575=COLOUR_RGB('Bearing light gray',0.725490196078431,0.752941176470588,
0.792156862745098);
ENDSEC;
END-ISO-10303-21;
